ISO-10303-21;
HEADER;
/* Generated by software containing ST-Developer
 * from STEP Tools, Inc. (www.steptools.com) 
 */

FILE_DESCRIPTION(
/* description */ ('Counterbalanced vertical column'),
/* implementation_level */ '2;1');

FILE_NAME(
/* name */ 'Cap Screw - M4x16.step',
/* time_stamp */ '2026-10-29T16:47:22-07:00',
/* author */ (''),
/* organization */ (''),
/* preprocessor_version */ 'ST-DEVELOPER v20.2',
/* originating_system */ 'Autodesk Translation Framework v15.17.0.0',
/* authorisation */ '');

FILE_SCHEMA (('AUTOMOTIVE_DESIGN { 1 0 10303 214 3 1 1 }'));
ENDSEC;

DATA;
#10=MECHANICAL_DESIGN_GEOMETRIC_PRESENTATION_REPRESENTATION('',(#384),#15040);
#258=CONICAL_SURFACE('',#8142,0.325,0.785398163397448);
#259=CONICAL_SURFACE('',#8146,0.335,0.785398163397448);
#260=CONICAL_SURFACE('',#8150,0.21,0.463647609000806);
#261=CONICAL_SURFACE('',#8154,0.18,0.785398163397448);
#265=ORIENTED_CLOSED_SHELL('',*,#7111,.F.);
#269=BREP_WITH_VOIDS('Body1',#7110,(#265));
#314=SHAPE_REPRESENTATION_RELATIONSHIP('SRR','None',#15220,#349);
#349=ADVANCED_BREP_SHAPE_REPRESENTATION('',(#269),#15039);
#384=STYLED_ITEM('',(#15464),#269);
#530=FACE_BOUND('',#1738,.T.);
#815=PLANE('',#8140);
#816=PLANE('',#8148);
#817=PLANE('',#8156);
#818=PLANE('',#8157);
#819=PLANE('',#8158);
#820=PLANE('',#8159);
#821=PLANE('',#8160);
#822=PLANE('',#8161);
#823=PLANE('',#8162);
#824=PLANE('',#8163);
#825=PLANE('',#8164);
#1214=FACE_OUTER_BOUND('',#1733,.T.);
#1215=FACE_OUTER_BOUND('',#1734,.T.);
#1216=FACE_OUTER_BOUND('',#1735,.T.);
#1217=FACE_OUTER_BOUND('',#1736,.T.);
#1218=FACE_OUTER_BOUND('',#1737,.T.);
#1219=FACE_OUTER_BOUND('',#1739,.T.);
#1220=FACE_OUTER_BOUND('',#1740,.T.);
#1221=FACE_OUTER_BOUND('',#1741,.T.);
#1222=FACE_OUTER_BOUND('',#1742,.T.);
#1223=FACE_OUTER_BOUND('',#1743,.T.);
#1224=FACE_OUTER_BOUND('',#1744,.T.);
#1225=FACE_OUTER_BOUND('',#1745,.T.);
#1226=FACE_OUTER_BOUND('',#1746,.T.);
#1227=FACE_OUTER_BOUND('',#1747,.T.);
#1228=FACE_OUTER_BOUND('',#1748,.T.);
#1229=FACE_OUTER_BOUND('',#1749,.T.);
#1230=FACE_OUTER_BOUND('',#1750,.T.);
#1733=EDGE_LOOP('',(#6510));
#1734=EDGE_LOOP('',(#6511,#6512,#6513,#6514));
#1735=EDGE_LOOP('',(#6515,#6516,#6517,#6518));
#1736=EDGE_LOOP('',(#6519,#6520,#6521,#6522));
#1737=EDGE_LOOP('',(#6523));
#1738=EDGE_LOOP('',(#6524));
#1739=EDGE_LOOP('',(#6525,#6526,#6527,#6528));
#1740=EDGE_LOOP('',(#6529,#6530,#6531,#6532));
#1741=EDGE_LOOP('',(#6533,#6534,#6535,#6536));
#1742=EDGE_LOOP('',(#6537));
#1743=EDGE_LOOP('',(#6538,#6539,#6540,#6541));
#1744=EDGE_LOOP('',(#6542,#6543,#6544,#6545));
#1745=EDGE_LOOP('',(#6546,#6547,#6548,#6549));
#1746=EDGE_LOOP('',(#6550,#6551,#6552,#6553));
#1747=EDGE_LOOP('',(#6554,#6555,#6556,#6557));
#1748=EDGE_LOOP('',(#6558,#6559,#6560,#6561));
#1749=EDGE_LOOP('',(#6562,#6563,#6564,#6565,#6566,#6567));
#1750=EDGE_LOOP('',(#6568,#6569,#6570,#6571,#6572,#6573));
#2398=LINE('',#14842,#3069);
#2399=LINE('',#14846,#3070);
#2400=LINE('',#14850,#3071);
#2401=LINE('',#14857,#3072);
#2402=LINE('',#14861,#3073);
#2403=LINE('',#14865,#3074);
#2404=LINE('',#14870,#3075);
#2405=LINE('',#14872,#3076);
#2406=LINE('',#14874,#3077);
#2407=LINE('',#14875,#3078);
#2408=LINE('',#14878,#3079);
#2409=LINE('',#14880,#3080);
#2410=LINE('',#14881,#3081);
#2411=LINE('',#14884,#3082);
#2412=LINE('',#14886,#3083);
#2413=LINE('',#14887,#3084);
#2414=LINE('',#14890,#3085);
#2415=LINE('',#14892,#3086);
#2416=LINE('',#14893,#3087);
#2417=LINE('',#14896,#3088);
#2418=LINE('',#14898,#3089);
#2419=LINE('',#14899,#3090);
#2420=LINE('',#14901,#3091);
#2421=LINE('',#14902,#3092);
#3069=VECTOR('',#10160,0.325);
#3070=VECTOR('',#10165,0.35);
#3071=VECTOR('',#10170,0.335);
#3072=VECTOR('',#10179,0.21);
#3073=VECTOR('',#10184,0.2);
#3074=VECTOR('',#10189,0.18);
#3075=VECTOR('',#10194,1.);
#3076=VECTOR('',#10195,1.);
#3077=VECTOR('',#10196,1.);
#3078=VECTOR('',#10197,1.);
#3079=VECTOR('',#10200,1.);
#3080=VECTOR('',#10201,1.);
#3081=VECTOR('',#10202,1.);
#3082=VECTOR('',#10205,1.);
#3083=VECTOR('',#10206,1.);
#3084=VECTOR('',#10207,1.);
#3085=VECTOR('',#10210,1.);
#3086=VECTOR('',#10211,1.);
#3087=VECTOR('',#10212,1.);
#3088=VECTOR('',#10215,1.);
#3089=VECTOR('',#10216,1.);
#3090=VECTOR('',#10217,1.);
#3091=VECTOR('',#10220,1.);
#3092=VECTOR('',#10221,1.);
#3298=CIRCLE('',#8141,0.3);
#3299=CIRCLE('',#8143,0.35);
#3300=CIRCLE('',#8145,0.35);
#3301=CIRCLE('',#8147,0.32);
#3302=CIRCLE('',#8149,0.22);
#3303=CIRCLE('',#8151,0.1954);
#3304=CIRCLE('',#8153,0.1954);
#3305=CIRCLE('',#8155,0.16);
#3875=VERTEX_POINT('',#14837);
#3876=VERTEX_POINT('',#14840);
#3877=VERTEX_POINT('',#14844);
#3878=VERTEX_POINT('',#14848);
#3879=VERTEX_POINT('',#14852);
#3880=VERTEX_POINT('',#14855);
#3881=VERTEX_POINT('',#14859);
#3882=VERTEX_POINT('',#14863);
#3883=VERTEX_POINT('',#14868);
#3884=VERTEX_POINT('',#14869);
#3885=VERTEX_POINT('',#14871);
#3886=VERTEX_POINT('',#14873);
#3887=VERTEX_POINT('',#14877);
#3888=VERTEX_POINT('',#14879);
#3889=VERTEX_POINT('',#14883);
#3890=VERTEX_POINT('',#14885);
#3891=VERTEX_POINT('',#14889);
#3892=VERTEX_POINT('',#14891);
#3893=VERTEX_POINT('',#14895);
#3894=VERTEX_POINT('',#14897);
#4756=EDGE_CURVE('',#3875,#3875,#3298,.T.);
#4757=EDGE_CURVE('',#3876,#3876,#3299,.T.);
#4758=EDGE_CURVE('',#3876,#3875,#2398,.T.);
#4759=EDGE_CURVE('',#3877,#3877,#3300,.T.);
#4760=EDGE_CURVE('',#3877,#3876,#2399,.T.);
#4761=EDGE_CURVE('',#3878,#3878,#3301,.T.);
#4762=EDGE_CURVE('',#3878,#3877,#2400,.T.);
#4763=EDGE_CURVE('',#3879,#3879,#3302,.T.);
#4764=EDGE_CURVE('',#3880,#3880,#3303,.F.);
#4765=EDGE_CURVE('',#3880,#3879,#2401,.T.);
#4766=EDGE_CURVE('',#3881,#3881,#3304,.F.);
#4767=EDGE_CURVE('',#3881,#3880,#2402,.T.);
#4768=EDGE_CURVE('',#3882,#3882,#3305,.T.);
#4769=EDGE_CURVE('',#3882,#3881,#2403,.T.);
#4770=EDGE_CURVE('',#3883,#3884,#2404,.T.);
#4771=EDGE_CURVE('',#3884,#3885,#2405,.T.);
#4772=EDGE_CURVE('',#3885,#3886,#2406,.T.);
#4773=EDGE_CURVE('',#3883,#3886,#2407,.T.);
#4774=EDGE_CURVE('',#3884,#3887,#2408,.T.);
#4775=EDGE_CURVE('',#3887,#3888,#2409,.T.);
#4776=EDGE_CURVE('',#3888,#3885,#2410,.T.);
#4777=EDGE_CURVE('',#3887,#3889,#2411,.T.);
#4778=EDGE_CURVE('',#3889,#3890,#2412,.T.);
#4779=EDGE_CURVE('',#3890,#3888,#2413,.T.);
#4780=EDGE_CURVE('',#3889,#3891,#2414,.T.);
#4781=EDGE_CURVE('',#3891,#3892,#2415,.T.);
#4782=EDGE_CURVE('',#3892,#3890,#2416,.T.);
#4783=EDGE_CURVE('',#3891,#3893,#2417,.T.);
#4784=EDGE_CURVE('',#3893,#3894,#2418,.T.);
#4785=EDGE_CURVE('',#3894,#3892,#2419,.T.);
#4786=EDGE_CURVE('',#3893,#3883,#2420,.T.);
#4787=EDGE_CURVE('',#3886,#3894,#2421,.T.);
#6510=ORIENTED_EDGE('',*,*,#4756,.F.);
#6511=ORIENTED_EDGE('',*,*,#4757,.F.);
#6512=ORIENTED_EDGE('',*,*,#4758,.T.);
#6513=ORIENTED_EDGE('',*,*,#4756,.T.);
#6514=ORIENTED_EDGE('',*,*,#4758,.F.);
#6515=ORIENTED_EDGE('',*,*,#4759,.F.);
#6516=ORIENTED_EDGE('',*,*,#4760,.T.);
#6517=ORIENTED_EDGE('',*,*,#4757,.T.);
#6518=ORIENTED_EDGE('',*,*,#4760,.F.);
#6519=ORIENTED_EDGE('',*,*,#4761,.F.);
#6520=ORIENTED_EDGE('',*,*,#4762,.T.);
#6521=ORIENTED_EDGE('',*,*,#4759,.T.);
#6522=ORIENTED_EDGE('',*,*,#4762,.F.);
#6523=ORIENTED_EDGE('',*,*,#4761,.T.);
#6524=ORIENTED_EDGE('',*,*,#4763,.F.);
#6525=ORIENTED_EDGE('',*,*,#4764,.F.);
#6526=ORIENTED_EDGE('',*,*,#4765,.T.);
#6527=ORIENTED_EDGE('',*,*,#4763,.T.);
#6528=ORIENTED_EDGE('',*,*,#4765,.F.);
#6529=ORIENTED_EDGE('',*,*,#4766,.F.);
#6530=ORIENTED_EDGE('',*,*,#4767,.T.);
#6531=ORIENTED_EDGE('',*,*,#4764,.T.);
#6532=ORIENTED_EDGE('',*,*,#4767,.F.);
#6533=ORIENTED_EDGE('',*,*,#4768,.F.);
#6534=ORIENTED_EDGE('',*,*,#4769,.T.);
#6535=ORIENTED_EDGE('',*,*,#4766,.T.);
#6536=ORIENTED_EDGE('',*,*,#4769,.F.);
#6537=ORIENTED_EDGE('',*,*,#4768,.T.);
#6538=ORIENTED_EDGE('',*,*,#4770,.T.);
#6539=ORIENTED_EDGE('',*,*,#4771,.T.);
#6540=ORIENTED_EDGE('',*,*,#4772,.T.);
#6541=ORIENTED_EDGE('',*,*,#4773,.F.);
#6542=ORIENTED_EDGE('',*,*,#4774,.T.);
#6543=ORIENTED_EDGE('',*,*,#4775,.T.);
#6544=ORIENTED_EDGE('',*,*,#4776,.T.);
#6545=ORIENTED_EDGE('',*,*,#4771,.F.);
#6546=ORIENTED_EDGE('',*,*,#4777,.T.);
#6547=ORIENTED_EDGE('',*,*,#4778,.T.);
#6548=ORIENTED_EDGE('',*,*,#4779,.T.);
#6549=ORIENTED_EDGE('',*,*,#4775,.F.);
#6550=ORIENTED_EDGE('',*,*,#4780,.T.);
#6551=ORIENTED_EDGE('',*,*,#4781,.T.);
#6552=ORIENTED_EDGE('',*,*,#4782,.T.);
#6553=ORIENTED_EDGE('',*,*,#4778,.F.);
#6554=ORIENTED_EDGE('',*,*,#4783,.T.);
#6555=ORIENTED_EDGE('',*,*,#4784,.T.);
#6556=ORIENTED_EDGE('',*,*,#4785,.T.);
#6557=ORIENTED_EDGE('',*,*,#4781,.F.);
#6558=ORIENTED_EDGE('',*,*,#4786,.T.);
#6559=ORIENTED_EDGE('',*,*,#4773,.T.);
#6560=ORIENTED_EDGE('',*,*,#4787,.T.);
#6561=ORIENTED_EDGE('',*,*,#4784,.F.);
#6562=ORIENTED_EDGE('',*,*,#4786,.F.);
#6563=ORIENTED_EDGE('',*,*,#4783,.F.);
#6564=ORIENTED_EDGE('',*,*,#4780,.F.);
#6565=ORIENTED_EDGE('',*,*,#4777,.F.);
#6566=ORIENTED_EDGE('',*,*,#4774,.F.);
#6567=ORIENTED_EDGE('',*,*,#4770,.F.);
#6568=ORIENTED_EDGE('',*,*,#4787,.F.);
#6569=ORIENTED_EDGE('',*,*,#4772,.F.);
#6570=ORIENTED_EDGE('',*,*,#4776,.F.);
#6571=ORIENTED_EDGE('',*,*,#4779,.F.);
#6572=ORIENTED_EDGE('',*,*,#4782,.F.);
#6573=ORIENTED_EDGE('',*,*,#4785,.F.);
#6666=CYLINDRICAL_SURFACE('',#8144,0.35);
#6667=CYLINDRICAL_SURFACE('',#8152,0.1954);
#7056=ADVANCED_FACE('',(#1214),#815,.T.);
#7057=ADVANCED_FACE('',(#1215),#258,.T.);
#7058=ADVANCED_FACE('',(#1216),#6666,.T.);
#7059=ADVANCED_FACE('',(#1217),#259,.T.);
#7060=ADVANCED_FACE('',(#1218,#530),#816,.T.);
#7061=ADVANCED_FACE('',(#1219),#260,.T.);
#7062=ADVANCED_FACE('',(#1220),#6667,.T.);
#7063=ADVANCED_FACE('',(#1221),#261,.T.);
#7064=ADVANCED_FACE('',(#1222),#817,.T.);
#7065=ADVANCED_FACE('',(#1223),#818,.F.);
#7066=ADVANCED_FACE('',(#1224),#819,.F.);
#7067=ADVANCED_FACE('',(#1225),#820,.F.);
#7068=ADVANCED_FACE('',(#1226),#821,.F.);
#7069=ADVANCED_FACE('',(#1227),#822,.F.);
#7070=ADVANCED_FACE('',(#1228),#823,.F.);
#7071=ADVANCED_FACE('',(#1229),#824,.F.);
#7072=ADVANCED_FACE('',(#1230),#825,.F.);
#7110=CLOSED_SHELL('',(#7056,#7057,#7058,#7059,#7060,#7061,#7062,#7063,
#7064));
#7111=CLOSED_SHELL('',(#7065,#7066,#7067,#7068,#7069,#7070,#7071,#7072));
#8139=AXIS2_PLACEMENT_3D('',#14835,#10150,#10151);
#8140=AXIS2_PLACEMENT_3D('',#14836,#10152,#10153);
#8141=AXIS2_PLACEMENT_3D('',#14838,#10154,#10155);
#8142=AXIS2_PLACEMENT_3D('',#14839,#10156,#10157);
#8143=AXIS2_PLACEMENT_3D('',#14841,#10158,#10159);
#8144=AXIS2_PLACEMENT_3D('',#14843,#10161,#10162);
#8145=AXIS2_PLACEMENT_3D('',#14845,#10163,#10164);
#8146=AXIS2_PLACEMENT_3D('',#14847,#10166,#10167);
#8147=AXIS2_PLACEMENT_3D('',#14849,#10168,#10169);
#8148=AXIS2_PLACEMENT_3D('',#14851,#10171,#10172);
#8149=AXIS2_PLACEMENT_3D('',#14853,#10173,#10174);
#8150=AXIS2_PLACEMENT_3D('',#14854,#10175,#10176);
#8151=AXIS2_PLACEMENT_3D('',#14856,#10177,#10178);
#8152=AXIS2_PLACEMENT_3D('',#14858,#10180,#10181);
#8153=AXIS2_PLACEMENT_3D('',#14860,#10182,#10183);
#8154=AXIS2_PLACEMENT_3D('',#14862,#10185,#10186);
#8155=AXIS2_PLACEMENT_3D('',#14864,#10187,#10188);
#8156=AXIS2_PLACEMENT_3D('',#14866,#10190,#10191);
#8157=AXIS2_PLACEMENT_3D('',#14867,#10192,#10193);
#8158=AXIS2_PLACEMENT_3D('',#14876,#10198,#10199);
#8159=AXIS2_PLACEMENT_3D('',#14882,#10203,#10204);
#8160=AXIS2_PLACEMENT_3D('',#14888,#10208,#10209);
#8161=AXIS2_PLACEMENT_3D('',#14894,#10213,#10214);
#8162=AXIS2_PLACEMENT_3D('',#14900,#10218,#10219);
#8163=AXIS2_PLACEMENT_3D('',#14903,#10222,#10223);
#8164=AXIS2_PLACEMENT_3D('',#14904,#10224,#10225);
#10150=DIRECTION('axis',(0.,0.,1.));
#10151=DIRECTION('refdir',(1.,0.,0.));
#10152=DIRECTION('center_axis',(0.,1.,0.));
#10153=DIRECTION('ref_axis',(0.,0.,1.));
#10154=DIRECTION('center_axis',(0.,-1.,0.));
#10155=DIRECTION('ref_axis',(1.,0.,0.));
#10156=DIRECTION('center_axis',(0.,-1.,0.));
#10157=DIRECTION('ref_axis',(1.,0.,0.));
#10158=DIRECTION('center_axis',(0.,-1.,0.));
#10159=DIRECTION('ref_axis',(1.,0.,0.));
#10160=DIRECTION('',(0.707106781186547,0.707106781186548,8.65956056235493E-17));
#10161=DIRECTION('center_axis',(0.,-1.,0.));
#10162=DIRECTION('ref_axis',(1.,0.,0.));
#10163=DIRECTION('center_axis',(0.,-1.,0.));
#10164=DIRECTION('ref_axis',(1.,0.,0.));
#10165=DIRECTION('',(0.,1.,0.));
#10166=DIRECTION('center_axis',(0.,1.,0.));
#10167=DIRECTION('ref_axis',(1.,0.,0.));
#10168=DIRECTION('center_axis',(0.,-1.,0.));
#10169=DIRECTION('ref_axis',(1.,0.,0.));
#10170=DIRECTION('',(-0.707106781186547,0.707106781186548,-8.65956056235493E-17));
#10171=DIRECTION('center_axis',(0.,-1.,0.));
#10172=DIRECTION('ref_axis',(0.,0.,-1.));
#10173=DIRECTION('center_axis',(0.,-1.,0.));
#10174=DIRECTION('ref_axis',(1.,0.,0.));
#10175=DIRECTION('center_axis',(0.,1.,0.));
#10176=DIRECTION('ref_axis',(1.,0.,0.));
#10177=DIRECTION('center_axis',(0.,1.,0.));
#10178=DIRECTION('ref_axis',(1.,0.,0.));
#10179=DIRECTION('',(-0.447213595499958,0.894427190999916,-5.47678698264203E-17));
#10180=DIRECTION('center_axis',(0.,-1.,0.));
#10181=DIRECTION('ref_axis',(1.,0.,0.));
#10182=DIRECTION('center_axis',(0.,1.,0.));
#10183=DIRECTION('ref_axis',(1.,0.,0.));
#10184=DIRECTION('',(0.,1.,0.));
#10185=DIRECTION('center_axis',(0.,1.,0.));
#10186=DIRECTION('ref_axis',(1.,0.,0.));
#10187=DIRECTION('center_axis',(0.,-1.,0.));
#10188=DIRECTION('ref_axis',(1.,0.,0.));
#10189=DIRECTION('',(-0.707106781186547,0.707106781186548,-8.65956056235493E-17));
#10190=DIRECTION('center_axis',(0.,-1.,0.));
#10191=DIRECTION('ref_axis',(0.,0.,-1.));
#10192=DIRECTION('center_axis',(0.866025403784439,0.,-0.5));
#10193=DIRECTION('ref_axis',(0.5,0.,0.866025403784439));
#10194=DIRECTION('',(-0.5,0.,-0.866025403784439));
#10195=DIRECTION('',(0.,-1.,0.));
#10196=DIRECTION('',(0.5,0.,0.866025403784439));
#10197=DIRECTION('',(0.,-1.,0.));
#10198=DIRECTION('center_axis',(1.60246890531964E-16,0.,-1.));
#10199=DIRECTION('ref_axis',(1.,0.,1.60246890531964E-16));
#10200=DIRECTION('',(-1.,0.,-1.60246890531964E-16));
#10201=DIRECTION('',(0.,-1.,0.));
#10202=DIRECTION('',(1.,0.,1.60246890531964E-16));
#10203=DIRECTION('center_axis',(-0.866025403784439,0.,-0.5));
#10204=DIRECTION('ref_axis',(0.5,0.,-0.866025403784439));
#10205=DIRECTION('',(-0.5,0.,0.866025403784439));
#10206=DIRECTION('',(0.,-1.,0.));
#10207=DIRECTION('',(0.5,0.,-0.866025403784439));
#10208=DIRECTION('center_axis',(-0.866025403784439,0.,0.5));
#10209=DIRECTION('ref_axis',(-0.5,0.,-0.866025403784439));
#10210=DIRECTION('',(0.5,0.,0.866025403784439));
#10211=DIRECTION('',(0.,-1.,0.));
#10212=DIRECTION('',(-0.5,0.,-0.866025403784439));
#10213=DIRECTION('center_axis',(-1.60246890531964E-16,0.,1.));
#10214=DIRECTION('ref_axis',(-1.,0.,-1.60246890531964E-16));
#10215=DIRECTION('',(1.,0.,1.60246890531964E-16));
#10216=DIRECTION('',(0.,-1.,0.));
#10217=DIRECTION('',(-1.,0.,-1.60246890531964E-16));
#10218=DIRECTION('center_axis',(0.866025403784439,0.,0.5));
#10219=DIRECTION('ref_axis',(-0.5,0.,0.866025403784439));
#10220=DIRECTION('',(0.5,0.,-0.866025403784439));
#10221=DIRECTION('',(-0.5,0.,0.866025403784439));
#10222=DIRECTION('center_axis',(0.,1.,0.));
#10223=DIRECTION('ref_axis',(1.,0.,0.));
#10224=DIRECTION('center_axis',(0.,-1.,0.));
#10225=DIRECTION('ref_axis',(0.,0.,-1.));
#14835=CARTESIAN_POINT('',(0.,0.,0.));
#14836=CARTESIAN_POINT('Origin',(0.3,0.4,0.));
#14837=CARTESIAN_POINT('',(-0.3,0.4,-3.67394039744206E-17));
#14838=CARTESIAN_POINT('Origin',(0.,0.4,0.));
#14839=CARTESIAN_POINT('Origin',(0.,0.375,0.));
#14840=CARTESIAN_POINT('',(-0.35,0.35,-4.28626379701573E-17));
#14841=CARTESIAN_POINT('Origin',(0.,0.35,0.));
#14842=CARTESIAN_POINT('',(-0.325,0.375,-3.9801020972289E-17));
#14843=CARTESIAN_POINT('Origin',(0.,0.19,0.));
#14844=CARTESIAN_POINT('',(-0.35,0.03,-4.28626379701574E-17));
#14845=CARTESIAN_POINT('Origin',(0.,0.03,0.));
#14846=CARTESIAN_POINT('',(-0.35,0.19,-4.28626379701574E-17));
#14847=CARTESIAN_POINT('Origin',(0.,0.0149999999999999,0.));
#14848=CARTESIAN_POINT('',(-0.32,-3.29597460435593E-17,-3.91886975727153E-17));
#14849=CARTESIAN_POINT('Origin',(0.,0.,0.));
#14850=CARTESIAN_POINT('',(-0.335,0.0149999999999999,-4.10256677714363E-17));
#14851=CARTESIAN_POINT('Origin',(0.22,0.,0.));
#14852=CARTESIAN_POINT('',(-0.22,-6.93889390390723E-18,-2.69422295812418E-17));
#14853=CARTESIAN_POINT('Origin',(0.,0.,0.));
#14854=CARTESIAN_POINT('Origin',(0.,-0.02,0.));
#14855=CARTESIAN_POINT('',(-0.1954,-0.0492,2.39295984553393E-17));
#14856=CARTESIAN_POINT('Origin',(0.,-0.0492,0.));
#14857=CARTESIAN_POINT('',(-0.21,-0.02,-2.57175827820944E-17));
#14858=CARTESIAN_POINT('Origin',(0.,-0.8,0.));
#14859=CARTESIAN_POINT('',(-0.1954,-1.5646,2.39295984553393E-17));
#14860=CARTESIAN_POINT('Origin',(0.,-1.5646,0.));
#14861=CARTESIAN_POINT('',(-0.1954,-0.8,-2.39295984553393E-17));
#14862=CARTESIAN_POINT('Origin',(0.,-1.58,0.));
#14863=CARTESIAN_POINT('',(-0.16,-1.6,-1.95943487863577E-17));
#14864=CARTESIAN_POINT('Origin',(0.,-1.6,0.));
#14865=CARTESIAN_POINT('',(-0.18,-1.58,-2.20436423846524E-17));
#14866=CARTESIAN_POINT('Origin',(0.,-1.6,0.));
#14867=CARTESIAN_POINT('Origin',(0.0866025403784439,-0.4,-0.15));
#14868=CARTESIAN_POINT('',(0.173205080756888,-0.4,0.));
#14869=CARTESIAN_POINT('',(0.0866025403784439,-0.4,-0.15));
#14870=CARTESIAN_POINT('',(0.173205080756888,-0.4,0.));
#14871=CARTESIAN_POINT('',(0.0866025403784439,-0.64,-0.15));
#14872=CARTESIAN_POINT('',(0.0866025403784439,-0.4,-0.15));
#14873=CARTESIAN_POINT('',(0.173205080756888,-0.64,0.));
#14874=CARTESIAN_POINT('',(0.173205080756888,-0.64,0.));
#14875=CARTESIAN_POINT('',(0.173205080756888,-0.4,0.));
#14876=CARTESIAN_POINT('Origin',(-0.0866025403784438,-0.4,-0.15));
#14877=CARTESIAN_POINT('',(-0.0866025403784438,-0.4,-0.15));
#14878=CARTESIAN_POINT('',(0.0866025403784439,-0.4,-0.15));
#14879=CARTESIAN_POINT('',(-0.0866025403784438,-0.64,-0.15));
#14880=CARTESIAN_POINT('',(-0.0866025403784438,-0.4,-0.15));
#14881=CARTESIAN_POINT('',(0.0866025403784439,-0.64,-0.15));
#14882=CARTESIAN_POINT('Origin',(-0.173205080756888,-0.4,-2.77555756156289E-17));
#14883=CARTESIAN_POINT('',(-0.173205080756888,-0.4,-2.12115047744981E-17));
#14884=CARTESIAN_POINT('',(-0.0866025403784438,-0.4,-0.15));
#14885=CARTESIAN_POINT('',(-0.173205080756888,-0.64,-2.77555756156289E-17));
#14886=CARTESIAN_POINT('',(-0.173205080756888,-0.4,-2.12115047744981E-17));
#14887=CARTESIAN_POINT('',(-0.0866025403784438,-0.64,-0.15));
#14888=CARTESIAN_POINT('Origin',(-0.0866025403784439,-0.4,0.15));
#14889=CARTESIAN_POINT('',(-0.0866025403784439,-0.4,0.15));
#14890=CARTESIAN_POINT('',(-0.173205080756888,-0.4,-2.12115047744981E-17));
#14891=CARTESIAN_POINT('',(-0.0866025403784439,-0.64,0.15));
#14892=CARTESIAN_POINT('',(-0.0866025403784439,-0.4,0.15));
#14893=CARTESIAN_POINT('',(-0.173205080756888,-0.64,-2.12115047744981E-17));
#14894=CARTESIAN_POINT('Origin',(0.0866025403784439,-0.4,0.15));
#14895=CARTESIAN_POINT('',(0.0866025403784439,-0.4,0.15));
#14896=CARTESIAN_POINT('',(-0.0866025403784439,-0.4,0.15));
#14897=CARTESIAN_POINT('',(0.0866025403784439,-0.64,0.15));
#14898=CARTESIAN_POINT('',(0.0866025403784439,-0.4,0.15));
#14899=CARTESIAN_POINT('',(-0.0866025403784439,-0.64,0.15));
#14900=CARTESIAN_POINT('Origin',(0.173205080756888,-0.4,0.));
#14901=CARTESIAN_POINT('',(0.0866025403784439,-0.4,0.15));
#14902=CARTESIAN_POINT('',(0.0866025403784439,-0.64,0.15));
#14903=CARTESIAN_POINT('Origin',(0.,-0.4,-2.77555756156289E-17));
#14904=CARTESIAN_POINT('Origin',(0.,-0.64,-2.77555756156289E-17));
#14999=UNCERTAINTY_MEASURE_WITH_UNIT(LENGTH_MEASURE(0.001),#15041,
'DISTANCE_ACCURACY_VALUE',
'Maximum model space distance between geometric entities at asserted c
onnectivities');
#15000=UNCERTAINTY_MEASURE_WITH_UNIT(LENGTH_MEASURE(0.001),#15041,
'DISTANCE_ACCURACY_VALUE',
'Maximum model space distance between geometric entities at asserted c
onnectivities');
#15039=(
GEOMETRIC_REPRESENTATION_CONTEXT(3)
GLOBAL_UNCERTAINTY_ASSIGNED_CONTEXT((#14999))
GLOBAL_UNIT_ASSIGNED_CONTEXT((#15041,#15043,#15044))
REPRESENTATION_CONTEXT('','3D')
);
#15040=(
GEOMETRIC_REPRESENTATION_CONTEXT(3)
GLOBAL_UNCERTAINTY_ASSIGNED_CONTEXT((#15000))
GLOBAL_UNIT_ASSIGNED_CONTEXT((#15041,#15043,#15044))
REPRESENTATION_CONTEXT('','3D')
);
#15041=(
LENGTH_UNIT()
NAMED_UNIT(*)
SI_UNIT(.CENTI.,.METRE.)
);
#15043=(
NAMED_UNIT(*)
PLANE_ANGLE_UNIT()
SI_UNIT($,.RADIAN.)
);
#15044=(
NAMED_UNIT(*)
SI_UNIT($,.STERADIAN.)
SOLID_ANGLE_UNIT()
);
#15083=SHAPE_DEFINITION_REPRESENTATION(#15125,#15220);
#15125=PRODUCT_DEFINITION_SHAPE('',$,#15260);
#15220=SHAPE_REPRESENTATION('',(#8139),#15039);
#15221=PRODUCT_DEFINITION_CONTEXT('part definition',#15340,'design');
#15260=PRODUCT_DEFINITION('Cap Screw - M4x16','Cap Screw - M4x16',#15299,
#15221);
#15299=PRODUCT_DEFINITION_FORMATION('',$,#15380);
#15340=APPLICATION_CONTEXT(
'Core Data for Automotive Mechanical Design Process');
#15341=PRODUCT_CONTEXT('part definition',#15340,'mechanical');
#15380=PRODUCT('Cap Screw - M4x16','Cap Screw - M4x16',
'Cap Screw - M4x16',(#15341));
#15458=COLOUR_RGB('Black',0.12,0.14,0.17);
#15459=FILL_AREA_STYLE_COLOUR('',#15458);
#15460=FILL_AREA_STYLE('',(#15459));
#15461=SURFACE_STYLE_FILL_AREA(#15460);
#15462=SURFACE_SIDE_STYLE('',(#15461));
#15463=SURFACE_STYLE_USAGE(.BOTH.,#15462);
#15464=PRESENTATION_STYLE_ASSIGNMENT((#15463));
ENDSEC;
END-ISO-10303-21;
